ISO-10303-21;
HEADER;
/* Generated by software containing ST-Developer
 * from STEP Tools, Inc. (www.steptools.com) 
 */

FILE_DESCRIPTION(
/* description */ ('Indexing fixture plate with plunger'),
/* implementation_level */ '2;1');

FILE_NAME(
/* name */ 'Cap Screw - M4x16.step',
/* time_stamp */ '2026-10-28T03:23:41-07:00',
/* author */ (''),
/* organization */ (''),
/* preprocessor_version */ 'ST-DEVELOPER v20.2',
/* originating_system */ 'Autodesk Translation Framework v15.17.0.0',
/* authorisation */ '');

FILE_SCHEMA (('AUTOMOTIVE_DESIGN { 1 0 10303 214 3 1 1 }'));
ENDSEC;

DATA;
#10=MECHANICAL_DESIGN_GEOMETRIC_PRESENTATION_REPRESENTATION('',(#349),#10020);
#223=CONICAL_SURFACE('',#5463,0.325,0.785398163397448);
#224=CONICAL_SURFACE('',#5467,0.335,0.785398163397448);
#225=CONICAL_SURFACE('',#5471,0.21,0.463647609000806);
#226=CONICAL_SURFACE('',#5475,0.18,0.785398163397448);
#230=ORIENTED_CLOSED_SHELL('',*,#4605,.F.);
#232=BREP_WITH_VOIDS('Body1',#4604,(#230));
#286=SHAPE_REPRESENTATION_RELATIONSHIP('SRR','None',#10162,#313);
#313=ADVANCED_BREP_SHAPE_REPRESENTATION('',(#232),#10015);
#349=STYLED_ITEM('',(#10375),#232);
#529=FACE_BOUND('',#1346,.T.);
#642=PLANE('',#5461);
#643=PLANE('',#5469);
#644=PLANE('',#5477);
#645=PLANE('',#5478);
#646=PLANE('',#5479);
#647=PLANE('',#5480);
#648=PLANE('',#5481);
#649=PLANE('',#5482);
#650=PLANE('',#5483);
#651=PLANE('',#5484);
#652=PLANE('',#5485);
#913=FACE_OUTER_BOUND('',#1341,.T.);
#914=FACE_OUTER_BOUND('',#1342,.T.);
#915=FACE_OUTER_BOUND('',#1343,.T.);
#916=FACE_OUTER_BOUND('',#1344,.T.);
#917=FACE_OUTER_BOUND('',#1345,.T.);
#918=FACE_OUTER_BOUND('',#1347,.T.);
#919=FACE_OUTER_BOUND('',#1348,.T.);
#920=FACE_OUTER_BOUND('',#1349,.T.);
#921=FACE_OUTER_BOUND('',#1350,.T.);
#922=FACE_OUTER_BOUND('',#1351,.T.);
#923=FACE_OUTER_BOUND('',#1352,.T.);
#924=FACE_OUTER_BOUND('',#1353,.T.);
#925=FACE_OUTER_BOUND('',#1354,.T.);
#926=FACE_OUTER_BOUND('',#1355,.T.);
#927=FACE_OUTER_BOUND('',#1356,.T.);
#928=FACE_OUTER_BOUND('',#1357,.T.);
#929=FACE_OUTER_BOUND('',#1358,.T.);
#1341=EDGE_LOOP('',(#4003));
#1342=EDGE_LOOP('',(#4004,#4005,#4006,#4007));
#1343=EDGE_LOOP('',(#4008,#4009,#4010,#4011));
#1344=EDGE_LOOP('',(#4012,#4013,#4014,#4015));
#1345=EDGE_LOOP('',(#4016));
#1346=EDGE_LOOP('',(#4017));
#1347=EDGE_LOOP('',(#4018,#4019,#4020,#4021));
#1348=EDGE_LOOP('',(#4022,#4023,#4024,#4025));
#1349=EDGE_LOOP('',(#4026,#4027,#4028,#4029));
#1350=EDGE_LOOP('',(#4030));
#1351=EDGE_LOOP('',(#4031,#4032,#4033,#4034));
#1352=EDGE_LOOP('',(#4035,#4036,#4037,#4038));
#1353=EDGE_LOOP('',(#4039,#4040,#4041,#4042));
#1354=EDGE_LOOP('',(#4043,#4044,#4045,#4046));
#1355=EDGE_LOOP('',(#4047,#4048,#4049,#4050));
#1356=EDGE_LOOP('',(#4051,#4052,#4053,#4054));
#1357=EDGE_LOOP('',(#4055,#4056,#4057,#4058,#4059,#4060));
#1358=EDGE_LOOP('',(#4061,#4062,#4063,#4064,#4065,#4066));
#1559=LINE('',#9693,#1779);
#1560=LINE('',#9697,#1780);
#1561=LINE('',#9701,#1781);
#1562=LINE('',#9708,#1782);
#1563=LINE('',#9712,#1783);
#1564=LINE('',#9716,#1784);
#1565=LINE('',#9721,#1785);
#1566=LINE('',#9723,#1786);
#1567=LINE('',#9725,#1787);
#1568=LINE('',#9726,#1788);
#1569=LINE('',#9729,#1789);
#1570=LINE('',#9731,#1790);
#1571=LINE('',#9732,#1791);
#1572=LINE('',#9735,#1792);
#1573=LINE('',#9737,#1793);
#1574=LINE('',#9738,#1794);
#1575=LINE('',#9741,#1795);
#1576=LINE('',#9743,#1796);
#1577=LINE('',#9744,#1797);
#1578=LINE('',#9747,#1798);
#1579=LINE('',#9749,#1799);
#1580=LINE('',#9750,#1800);
#1581=LINE('',#9752,#1801);
#1582=LINE('',#9753,#1802);
#1779=VECTOR('',#6856,0.325);
#1780=VECTOR('',#6861,0.35);
#1781=VECTOR('',#6866,0.335);
#1782=VECTOR('',#6875,0.21);
#1783=VECTOR('',#6880,0.2);
#1784=VECTOR('',#6885,0.18);
#1785=VECTOR('',#6890,1.);
#1786=VECTOR('',#6891,1.);
#1787=VECTOR('',#6892,1.);
#1788=VECTOR('',#6893,1.);
#1789=VECTOR('',#6896,1.);
#1790=VECTOR('',#6897,1.);
#1791=VECTOR('',#6898,1.);
#1792=VECTOR('',#6901,1.);
#1793=VECTOR('',#6902,1.);
#1794=VECTOR('',#6903,1.);
#1795=VECTOR('',#6906,1.);
#1796=VECTOR('',#6907,1.);
#1797=VECTOR('',#6908,1.);
#1798=VECTOR('',#6911,1.);
#1799=VECTOR('',#6912,1.);
#1800=VECTOR('',#6913,1.);
#1801=VECTOR('',#6916,1.);
#1802=VECTOR('',#6917,1.);
#2111=CIRCLE('',#5462,0.3);
#2112=CIRCLE('',#5464,0.35);
#2113=CIRCLE('',#5466,0.35);
#2114=CIRCLE('',#5468,0.32);
#2115=CIRCLE('',#5470,0.22);
#2116=CIRCLE('',#5472,0.1954);
#2117=CIRCLE('',#5474,0.1954);
#2118=CIRCLE('',#5476,0.16);
#2458=VERTEX_POINT('',#9688);
#2459=VERTEX_POINT('',#9691);
#2460=VERTEX_POINT('',#9695);
#2461=VERTEX_POINT('',#9699);
#2462=VERTEX_POINT('',#9703);
#2463=VERTEX_POINT('',#9706);
#2464=VERTEX_POINT('',#9710);
#2465=VERTEX_POINT('',#9714);
#2466=VERTEX_POINT('',#9719);
#2467=VERTEX_POINT('',#9720);
#2468=VERTEX_POINT('',#9722);
#2469=VERTEX_POINT('',#9724);
#2470=VERTEX_POINT('',#9728);
#2471=VERTEX_POINT('',#9730);
#2472=VERTEX_POINT('',#9734);
#2473=VERTEX_POINT('',#9736);
#2474=VERTEX_POINT('',#9740);
#2475=VERTEX_POINT('',#9742);
#2476=VERTEX_POINT('',#9746);
#2477=VERTEX_POINT('',#9748);
#2981=EDGE_CURVE('',#2458,#2458,#2111,.T.);
#2982=EDGE_CURVE('',#2459,#2459,#2112,.T.);
#2983=EDGE_CURVE('',#2459,#2458,#1559,.T.);
#2984=EDGE_CURVE('',#2460,#2460,#2113,.T.);
#2985=EDGE_CURVE('',#2460,#2459,#1560,.T.);
#2986=EDGE_CURVE('',#2461,#2461,#2114,.T.);
#2987=EDGE_CURVE('',#2461,#2460,#1561,.T.);
#2988=EDGE_CURVE('',#2462,#2462,#2115,.T.);
#2989=EDGE_CURVE('',#2463,#2463,#2116,.F.);
#2990=EDGE_CURVE('',#2463,#2462,#1562,.T.);
#2991=EDGE_CURVE('',#2464,#2464,#2117,.F.);
#2992=EDGE_CURVE('',#2464,#2463,#1563,.T.);
#2993=EDGE_CURVE('',#2465,#2465,#2118,.T.);
#2994=EDGE_CURVE('',#2465,#2464,#1564,.T.);
#2995=EDGE_CURVE('',#2466,#2467,#1565,.T.);
#2996=EDGE_CURVE('',#2467,#2468,#1566,.T.);
#2997=EDGE_CURVE('',#2468,#2469,#1567,.T.);
#2998=EDGE_CURVE('',#2466,#2469,#1568,.T.);
#2999=EDGE_CURVE('',#2467,#2470,#1569,.T.);
#3000=EDGE_CURVE('',#2470,#2471,#1570,.T.);
#3001=EDGE_CURVE('',#2471,#2468,#1571,.T.);
#3002=EDGE_CURVE('',#2470,#2472,#1572,.T.);
#3003=EDGE_CURVE('',#2472,#2473,#1573,.T.);
#3004=EDGE_CURVE('',#2473,#2471,#1574,.T.);
#3005=EDGE_CURVE('',#2472,#2474,#1575,.T.);
#3006=EDGE_CURVE('',#2474,#2475,#1576,.T.);
#3007=EDGE_CURVE('',#2475,#2473,#1577,.T.);
#3008=EDGE_CURVE('',#2474,#2476,#1578,.T.);
#3009=EDGE_CURVE('',#2476,#2477,#1579,.T.);
#3010=EDGE_CURVE('',#2477,#2475,#1580,.T.);
#3011=EDGE_CURVE('',#2476,#2466,#1581,.T.);
#3012=EDGE_CURVE('',#2469,#2477,#1582,.T.);
#4003=ORIENTED_EDGE('',*,*,#2981,.F.);
#4004=ORIENTED_EDGE('',*,*,#2982,.F.);
#4005=ORIENTED_EDGE('',*,*,#2983,.T.);
#4006=ORIENTED_EDGE('',*,*,#2981,.T.);
#4007=ORIENTED_EDGE('',*,*,#2983,.F.);
#4008=ORIENTED_EDGE('',*,*,#2984,.F.);
#4009=ORIENTED_EDGE('',*,*,#2985,.T.);
#4010=ORIENTED_EDGE('',*,*,#2982,.T.);
#4011=ORIENTED_EDGE('',*,*,#2985,.F.);
#4012=ORIENTED_EDGE('',*,*,#2986,.F.);
#4013=ORIENTED_EDGE('',*,*,#2987,.T.);
#4014=ORIENTED_EDGE('',*,*,#2984,.T.);
#4015=ORIENTED_EDGE('',*,*,#2987,.F.);
#4016=ORIENTED_EDGE('',*,*,#2986,.T.);
#4017=ORIENTED_EDGE('',*,*,#2988,.F.);
#4018=ORIENTED_EDGE('',*,*,#2989,.F.);
#4019=ORIENTED_EDGE('',*,*,#2990,.T.);
#4020=ORIENTED_EDGE('',*,*,#2988,.T.);
#4021=ORIENTED_EDGE('',*,*,#2990,.F.);
#4022=ORIENTED_EDGE('',*,*,#2991,.F.);
#4023=ORIENTED_EDGE('',*,*,#2992,.T.);
#4024=ORIENTED_EDGE('',*,*,#2989,.T.);
#4025=ORIENTED_EDGE('',*,*,#2992,.F.);
#4026=ORIENTED_EDGE('',*,*,#2993,.F.);
#4027=ORIENTED_EDGE('',*,*,#2994,.T.);
#4028=ORIENTED_EDGE('',*,*,#2991,.T.);
#4029=ORIENTED_EDGE('',*,*,#2994,.F.);
#4030=ORIENTED_EDGE('',*,*,#2993,.T.);
#4031=ORIENTED_EDGE('',*,*,#2995,.T.);
#4032=ORIENTED_EDGE('',*,*,#2996,.T.);
#4033=ORIENTED_EDGE('',*,*,#2997,.T.);
#4034=ORIENTED_EDGE('',*,*,#2998,.F.);
#4035=ORIENTED_EDGE('',*,*,#2999,.T.);
#4036=ORIENTED_EDGE('',*,*,#3000,.T.);
#4037=ORIENTED_EDGE('',*,*,#3001,.T.);
#4038=ORIENTED_EDGE('',*,*,#2996,.F.);
#4039=ORIENTED_EDGE('',*,*,#3002,.T.);
#4040=ORIENTED_EDGE('',*,*,#3003,.T.);
#4041=ORIENTED_EDGE('',*,*,#3004,.T.);
#4042=ORIENTED_EDGE('',*,*,#3000,.F.);
#4043=ORIENTED_EDGE('',*,*,#3005,.T.);
#4044=ORIENTED_EDGE('',*,*,#3006,.T.);
#4045=ORIENTED_EDGE('',*,*,#3007,.T.);
#4046=ORIENTED_EDGE('',*,*,#3003,.F.);
#4047=ORIENTED_EDGE('',*,*,#3008,.T.);
#4048=ORIENTED_EDGE('',*,*,#3009,.T.);
#4049=ORIENTED_EDGE('',*,*,#3010,.T.);
#4050=ORIENTED_EDGE('',*,*,#3006,.F.);
#4051=ORIENTED_EDGE('',*,*,#3011,.T.);
#4052=ORIENTED_EDGE('',*,*,#2998,.T.);
#4053=ORIENTED_EDGE('',*,*,#3012,.T.);
#4054=ORIENTED_EDGE('',*,*,#3009,.F.);
#4055=ORIENTED_EDGE('',*,*,#3011,.F.);
#4056=ORIENTED_EDGE('',*,*,#3008,.F.);
#4057=ORIENTED_EDGE('',*,*,#3005,.F.);
#4058=ORIENTED_EDGE('',*,*,#3002,.F.);
#4059=ORIENTED_EDGE('',*,*,#2999,.F.);
#4060=ORIENTED_EDGE('',*,*,#2995,.F.);
#4061=ORIENTED_EDGE('',*,*,#3012,.F.);
#4062=ORIENTED_EDGE('',*,*,#2997,.F.);
#4063=ORIENTED_EDGE('',*,*,#3001,.F.);
#4064=ORIENTED_EDGE('',*,*,#3004,.F.);
#4065=ORIENTED_EDGE('',*,*,#3007,.F.);
#4066=ORIENTED_EDGE('',*,*,#3010,.F.);
#4276=CYLINDRICAL_SURFACE('',#5465,0.35);
#4277=CYLINDRICAL_SURFACE('',#5473,0.1954);
#4528=ADVANCED_FACE('',(#913),#642,.T.);
#4529=ADVANCED_FACE('',(#914),#223,.T.);
#4530=ADVANCED_FACE('',(#915),#4276,.T.);
#4531=ADVANCED_FACE('',(#916),#224,.T.);
#4532=ADVANCED_FACE('',(#917,#529),#643,.T.);
#4533=ADVANCED_FACE('',(#918),#225,.T.);
#4534=ADVANCED_FACE('',(#919),#4277,.T.);
#4535=ADVANCED_FACE('',(#920),#226,.T.);
#4536=ADVANCED_FACE('',(#921),#644,.T.);
#4537=ADVANCED_FACE('',(#922),#645,.F.);
#4538=ADVANCED_FACE('',(#923),#646,.F.);
#4539=ADVANCED_FACE('',(#924),#647,.F.);
#4540=ADVANCED_FACE('',(#925),#648,.F.);
#4541=ADVANCED_FACE('',(#926),#649,.F.);
#4542=ADVANCED_FACE('',(#927),#650,.F.);
#4543=ADVANCED_FACE('',(#928),#651,.F.);
#4544=ADVANCED_FACE('',(#929),#652,.F.);
#4604=CLOSED_SHELL('',(#4528,#4529,#4530,#4531,#4532,#4533,#4534,#4535,
#4536));
#4605=CLOSED_SHELL('',(#4537,#4538,#4539,#4540,#4541,#4542,#4543,#4544));
#5460=AXIS2_PLACEMENT_3D('',#9686,#6846,#6847);
#5461=AXIS2_PLACEMENT_3D('',#9687,#6848,#6849);
#5462=AXIS2_PLACEMENT_3D('',#9689,#6850,#6851);
#5463=AXIS2_PLACEMENT_3D('',#9690,#6852,#6853);
#5464=AXIS2_PLACEMENT_3D('',#9692,#6854,#6855);
#5465=AXIS2_PLACEMENT_3D('',#9694,#6857,#6858);
#5466=AXIS2_PLACEMENT_3D('',#9696,#6859,#6860);
#5467=AXIS2_PLACEMENT_3D('',#9698,#6862,#6863);
#5468=AXIS2_PLACEMENT_3D('',#9700,#6864,#6865);
#5469=AXIS2_PLACEMENT_3D('',#9702,#6867,#6868);
#5470=AXIS2_PLACEMENT_3D('',#9704,#6869,#6870);
#5471=AXIS2_PLACEMENT_3D('',#9705,#6871,#6872);
#5472=AXIS2_PLACEMENT_3D('',#9707,#6873,#6874);
#5473=AXIS2_PLACEMENT_3D('',#9709,#6876,#6877);
#5474=AXIS2_PLACEMENT_3D('',#9711,#6878,#6879);
#5475=AXIS2_PLACEMENT_3D('',#9713,#6881,#6882);
#5476=AXIS2_PLACEMENT_3D('',#9715,#6883,#6884);
#5477=AXIS2_PLACEMENT_3D('',#9717,#6886,#6887);
#5478=AXIS2_PLACEMENT_3D('',#9718,#6888,#6889);
#5479=AXIS2_PLACEMENT_3D('',#9727,#6894,#6895);
#5480=AXIS2_PLACEMENT_3D('',#9733,#6899,#6900);
#5481=AXIS2_PLACEMENT_3D('',#9739,#6904,#6905);
#5482=AXIS2_PLACEMENT_3D('',#9745,#6909,#6910);
#5483=AXIS2_PLACEMENT_3D('',#9751,#6914,#6915);
#5484=AXIS2_PLACEMENT_3D('',#9754,#6918,#6919);
#5485=AXIS2_PLACEMENT_3D('',#9755,#6920,#6921);
#6846=DIRECTION('axis',(0.,0.,1.));
#6847=DIRECTION('refdir',(1.,0.,0.));
#6848=DIRECTION('center_axis',(0.,1.,0.));
#6849=DIRECTION('ref_axis',(0.,0.,1.));
#6850=DIRECTION('center_axis',(0.,-1.,0.));
#6851=DIRECTION('ref_axis',(1.,0.,0.));
#6852=DIRECTION('center_axis',(0.,-1.,0.));
#6853=DIRECTION('ref_axis',(1.,0.,0.));
#6854=DIRECTION('center_axis',(0.,-1.,0.));
#6855=DIRECTION('ref_axis',(1.,0.,0.));
#6856=DIRECTION('',(0.707106781186547,0.707106781186548,8.65956056235493E-17));
#6857=DIRECTION('center_axis',(0.,-1.,0.));
#6858=DIRECTION('ref_axis',(1.,0.,0.));
#6859=DIRECTION('center_axis',(0.,-1.,0.));
#6860=DIRECTION('ref_axis',(1.,0.,0.));
#6861=DIRECTION('',(0.,1.,0.));
#6862=DIRECTION('center_axis',(0.,1.,0.));
#6863=DIRECTION('ref_axis',(1.,0.,0.));
#6864=DIRECTION('center_axis',(0.,-1.,0.));
#6865=DIRECTION('ref_axis',(1.,0.,0.));
#6866=DIRECTION('',(-0.707106781186547,0.707106781186548,-8.65956056235493E-17));
#6867=DIRECTION('center_axis',(0.,-1.,0.));
#6868=DIRECTION('ref_axis',(0.,0.,-1.));
#6869=DIRECTION('center_axis',(0.,-1.,0.));
#6870=DIRECTION('ref_axis',(1.,0.,0.));
#6871=DIRECTION('center_axis',(0.,1.,0.));
#6872=DIRECTION('ref_axis',(1.,0.,0.));
#6873=DIRECTION('center_axis',(0.,1.,0.));
#6874=DIRECTION('ref_axis',(1.,0.,0.));
#6875=DIRECTION('',(-0.447213595499958,0.894427190999916,-5.47678698264203E-17));
#6876=DIRECTION('center_axis',(0.,-1.,0.));
#6877=DIRECTION('ref_axis',(1.,0.,0.));
#6878=DIRECTION('center_axis',(0.,1.,0.));
#6879=DIRECTION('ref_axis',(1.,0.,0.));
#6880=DIRECTION('',(0.,1.,0.));
#6881=DIRECTION('center_axis',(0.,1.,0.));
#6882=DIRECTION('ref_axis',(1.,0.,0.));
#6883=DIRECTION('center_axis',(0.,-1.,0.));
#6884=DIRECTION('ref_axis',(1.,0.,0.));
#6885=DIRECTION('',(-0.707106781186547,0.707106781186548,-8.65956056235493E-17));
#6886=DIRECTION('center_axis',(0.,-1.,0.));
#6887=DIRECTION('ref_axis',(0.,0.,-1.));
#6888=DIRECTION('center_axis',(0.866025403784439,0.,-0.5));
#6889=DIRECTION('ref_axis',(0.5,0.,0.866025403784439));
#6890=DIRECTION('',(-0.5,0.,-0.866025403784439));
#6891=DIRECTION('',(0.,-1.,0.));
#6892=DIRECTION('',(0.5,0.,0.866025403784439));
#6893=DIRECTION('',(0.,-1.,0.));
#6894=DIRECTION('center_axis',(1.60246890531964E-16,0.,-1.));
#6895=DIRECTION('ref_axis',(1.,0.,1.60246890531964E-16));
#6896=DIRECTION('',(-1.,0.,-1.60246890531964E-16));
#6897=DIRECTION('',(0.,-1.,0.));
#6898=DIRECTION('',(1.,0.,1.60246890531964E-16));
#6899=DIRECTION('center_axis',(-0.866025403784439,0.,-0.5));
#6900=DIRECTION('ref_axis',(0.5,0.,-0.866025403784439));
#6901=DIRECTION('',(-0.5,0.,0.866025403784439));
#6902=DIRECTION('',(0.,-1.,0.));
#6903=DIRECTION('',(0.5,0.,-0.866025403784439));
#6904=DIRECTION('center_axis',(-0.866025403784439,0.,0.5));
#6905=DIRECTION('ref_axis',(-0.5,0.,-0.866025403784439));
#6906=DIRECTION('',(0.5,0.,0.866025403784439));
#6907=DIRECTION('',(0.,-1.,0.));
#6908=DIRECTION('',(-0.5,0.,-0.866025403784439));
#6909=DIRECTION('center_axis',(-1.60246890531964E-16,0.,1.));
#6910=DIRECTION('ref_axis',(-1.,0.,-1.60246890531964E-16));
#6911=DIRECTION('',(1.,0.,1.60246890531964E-16));
#6912=DIRECTION('',(0.,-1.,0.));
#6913=DIRECTION('',(-1.,0.,-1.60246890531964E-16));
#6914=DIRECTION('center_axis',(0.866025403784439,0.,0.5));
#6915=DIRECTION('ref_axis',(-0.5,0.,0.866025403784439));
#6916=DIRECTION('',(0.5,0.,-0.866025403784439));
#6917=DIRECTION('',(-0.5,0.,0.866025403784439));
#6918=DIRECTION('center_axis',(0.,1.,0.));
#6919=DIRECTION('ref_axis',(1.,0.,0.));
#6920=DIRECTION('center_axis',(0.,-1.,0.));
#6921=DIRECTION('ref_axis',(0.,0.,-1.));
#9686=CARTESIAN_POINT('',(0.,0.,0.));
#9687=CARTESIAN_POINT('Origin',(0.3,0.4,0.));
#9688=CARTESIAN_POINT('',(-0.3,0.4,-3.67394039744206E-17));
#9689=CARTESIAN_POINT('Origin',(0.,0.4,0.));
#9690=CARTESIAN_POINT('Origin',(0.,0.375,0.));
#9691=CARTESIAN_POINT('',(-0.35,0.35,-4.28626379701573E-17));
#9692=CARTESIAN_POINT('Origin',(0.,0.35,0.));
#9693=CARTESIAN_POINT('',(-0.325,0.375,-3.9801020972289E-17));
#9694=CARTESIAN_POINT('Origin',(0.,0.19,0.));
#9695=CARTESIAN_POINT('',(-0.35,0.03,-4.28626379701574E-17));
#9696=CARTESIAN_POINT('Origin',(0.,0.03,0.));
#9697=CARTESIAN_POINT('',(-0.35,0.19,-4.28626379701574E-17));
#9698=CARTESIAN_POINT('Origin',(0.,0.0149999999999999,0.));
#9699=CARTESIAN_POINT('',(-0.32,-3.29597460435593E-17,-3.91886975727153E-17));
#9700=CARTESIAN_POINT('Origin',(0.,0.,0.));
#9701=CARTESIAN_POINT('',(-0.335,0.0149999999999999,-4.10256677714363E-17));
#9702=CARTESIAN_POINT('Origin',(0.22,0.,0.));
#9703=CARTESIAN_POINT('',(-0.22,-6.93889390390723E-18,-2.69422295812418E-17));
#9704=CARTESIAN_POINT('Origin',(0.,0.,0.));
#9705=CARTESIAN_POINT('Origin',(0.,-0.02,0.));
#9706=CARTESIAN_POINT('',(-0.1954,-0.0492,2.39295984553393E-17));
#9707=CARTESIAN_POINT('Origin',(0.,-0.0492,0.));
#9708=CARTESIAN_POINT('',(-0.21,-0.02,-2.57175827820944E-17));
#9709=CARTESIAN_POINT('Origin',(0.,-0.8,0.));
#9710=CARTESIAN_POINT('',(-0.1954,-1.5646,2.39295984553393E-17));
#9711=CARTESIAN_POINT('Origin',(0.,-1.5646,0.));
#9712=CARTESIAN_POINT('',(-0.1954,-0.8,-2.39295984553393E-17));
#9713=CARTESIAN_POINT('Origin',(0.,-1.58,0.));
#9714=CARTESIAN_POINT('',(-0.16,-1.6,-1.95943487863577E-17));
#9715=CARTESIAN_POINT('Origin',(0.,-1.6,0.));
#9716=CARTESIAN_POINT('',(-0.18,-1.58,-2.20436423846524E-17));
#9717=CARTESIAN_POINT('Origin',(0.,-1.6,0.));
#9718=CARTESIAN_POINT('Origin',(0.0866025403784439,-0.4,-0.15));
#9719=CARTESIAN_POINT('',(0.173205080756888,-0.4,0.));
#9720=CARTESIAN_POINT('',(0.0866025403784439,-0.4,-0.15));
#9721=CARTESIAN_POINT('',(0.173205080756888,-0.4,0.));
#9722=CARTESIAN_POINT('',(0.0866025403784439,-0.64,-0.15));
#9723=CARTESIAN_POINT('',(0.0866025403784439,-0.4,-0.15));
#9724=CARTESIAN_POINT('',(0.173205080756888,-0.64,0.));
#9725=CARTESIAN_POINT('',(0.173205080756888,-0.64,0.));
#9726=CARTESIAN_POINT('',(0.173205080756888,-0.4,0.));
#9727=CARTESIAN_POINT('Origin',(-0.0866025403784438,-0.4,-0.15));
#9728=CARTESIAN_POINT('',(-0.0866025403784438,-0.4,-0.15));
#9729=CARTESIAN_POINT('',(0.0866025403784439,-0.4,-0.15));
#9730=CARTESIAN_POINT('',(-0.0866025403784438,-0.64,-0.15));
#9731=CARTESIAN_POINT('',(-0.0866025403784438,-0.4,-0.15));
#9732=CARTESIAN_POINT('',(0.0866025403784439,-0.64,-0.15));
#9733=CARTESIAN_POINT('Origin',(-0.173205080756888,-0.4,-2.77555756156289E-17));
#9734=CARTESIAN_POINT('',(-0.173205080756888,-0.4,-2.12115047744981E-17));
#9735=CARTESIAN_POINT('',(-0.0866025403784438,-0.4,-0.15));
#9736=CARTESIAN_POINT('',(-0.173205080756888,-0.64,-2.77555756156289E-17));
#9737=CARTESIAN_POINT('',(-0.173205080756888,-0.4,-2.12115047744981E-17));
#9738=CARTESIAN_POINT('',(-0.0866025403784438,-0.64,-0.15));
#9739=CARTESIAN_POINT('Origin',(-0.0866025403784439,-0.4,0.15));
#9740=CARTESIAN_POINT('',(-0.0866025403784439,-0.4,0.15));
#9741=CARTESIAN_POINT('',(-0.173205080756888,-0.4,-2.12115047744981E-17));
#9742=CARTESIAN_POINT('',(-0.0866025403784439,-0.64,0.15));
#9743=CARTESIAN_POINT('',(-0.0866025403784439,-0.4,0.15));
#9744=CARTESIAN_POINT('',(-0.173205080756888,-0.64,-2.12115047744981E-17));
#9745=CARTESIAN_POINT('Origin',(0.0866025403784439,-0.4,0.15));
#9746=CARTESIAN_POINT('',(0.0866025403784439,-0.4,0.15));
#9747=CARTESIAN_POINT('',(-0.0866025403784439,-0.4,0.15));
#9748=CARTESIAN_POINT('',(0.0866025403784439,-0.64,0.15));
#9749=CARTESIAN_POINT('',(0.0866025403784439,-0.4,0.15));
#9750=CARTESIAN_POINT('',(-0.0866025403784439,-0.64,0.15));
#9751=CARTESIAN_POINT('Origin',(0.173205080756888,-0.4,0.));
#9752=CARTESIAN_POINT('',(0.0866025403784439,-0.4,0.15));
#9753=CARTESIAN_POINT('',(0.0866025403784439,-0.64,0.15));
#9754=CARTESIAN_POINT('Origin',(0.,-0.4,-2.77555756156289E-17));
#9755=CARTESIAN_POINT('Origin',(0.,-0.64,-2.77555756156289E-17));
#9982=UNCERTAINTY_MEASURE_WITH_UNIT(LENGTH_MEASURE(0.001),#10021,
'DISTANCE_ACCURACY_VALUE',
'Maximum model space distance between geometric entities at asserted c
onnectivities');
#9987=UNCERTAINTY_MEASURE_WITH_UNIT(LENGTH_MEASURE(0.001),#10021,
'DISTANCE_ACCURACY_VALUE',
'Maximum model space distance between geometric entities at asserted c
onnectivities');
#10015=(
GEOMETRIC_REPRESENTATION_CONTEXT(3)
GLOBAL_UNCERTAINTY_ASSIGNED_CONTEXT((#9982))
GLOBAL_UNIT_ASSIGNED_CONTEXT((#10021,#10023,#10024))
REPRESENTATION_CONTEXT('','3D')
);
#10020=(
GEOMETRIC_REPRESENTATION_CONTEXT(3)
GLOBAL_UNCERTAINTY_ASSIGNED_CONTEXT((#9987))
GLOBAL_UNIT_ASSIGNED_CONTEXT((#10021,#10023,#10024))
REPRESENTATION_CONTEXT('','3D')
);
#10021=(
LENGTH_UNIT()
NAMED_UNIT(*)
SI_UNIT(.CENTI.,.METRE.)
);
#10023=(
NAMED_UNIT(*)
PLANE_ANGLE_UNIT()
SI_UNIT($,.RADIAN.)
);
#10024=(
NAMED_UNIT(*)
SI_UNIT($,.STERADIAN.)
SOLID_ANGLE_UNIT()
);
#10052=SHAPE_DEFINITION_REPRESENTATION(#10089,#10162);
#10089=PRODUCT_DEFINITION_SHAPE('',$,#10195);
#10162=SHAPE_REPRESENTATION('',(#5460),#10015);
#10167=PRODUCT_DEFINITION_CONTEXT('part definition',#10265,'design');
#10195=PRODUCT_DEFINITION('Cap Screw - M4x16','Cap Screw - M4x16',#10227,
#10167);
#10227=PRODUCT_DEFINITION_FORMATION('',$,#10294);
#10265=APPLICATION_CONTEXT(
'Core Data for Automotive Mechanical Design Process');
#10266=PRODUCT_CONTEXT('part definition',#10265,'mechanical');
#10294=PRODUCT('Cap Screw - M4x16','Cap Screw - M4x16',
'Cap Screw - M4x16',(#10266));
#10369=COLOUR_RGB('Black',0.12,0.14,0.17);
#10370=FILL_AREA_STYLE_COLOUR('',#10369);
#10371=FILL_AREA_STYLE('',(#10370));
#10372=SURFACE_STYLE_FILL_AREA(#10371);
#10373=SURFACE_SIDE_STYLE('',(#10372));
#10374=SURFACE_STYLE_USAGE(.BOTH.,#10373);
#10375=PRESENTATION_STYLE_ASSIGNMENT((#10374));
ENDSEC;
END-ISO-10303-21;
